ISO-10303-21;
HEADER;
/* Generated by software containing ST-Developer
 * from STEP Tools, Inc. (www.steptools.com) 
 */

FILE_DESCRIPTION(
/* description */ ('Round-Shaft Linear Stage with Ball Bushings'),
/* implementation_level */ '2;1');

FILE_NAME(
/* name */ 'Flat Washer - M6.step',
/* time_stamp */ '2026-10-27T10:47:55-07:00',
/* author */ (''),
/* organization */ (''),
/* preprocessor_version */ 'ST-DEVELOPER v20.2',
/* originating_system */ 'Autodesk Translation Framework v15.17.0.0',
/* authorisation */ '');

FILE_SCHEMA (('AUTOMOTIVE_DESIGN { 1 0 10303 214 3 1 1 }'));
ENDSEC;

DATA;
#10=MECHANICAL_DESIGN_GEOMETRIC_PRESENTATION_REPRESENTATION('',(#321),#7835);
#279=SHAPE_REPRESENTATION_RELATIONSHIP('SRR','None',#7969,#300);
#300=ADVANCED_BREP_SHAPE_REPRESENTATION('',(#339),#7833);
#321=STYLED_ITEM('',(#8151),#339);
#339=MANIFOLD_SOLID_BREP('Body1',#4414);
#456=FACE_BOUND('',#1228,.T.);
#457=FACE_BOUND('',#1230,.T.);
#603=PLANE('',#5121);
#604=PLANE('',#5122);
#852=FACE_OUTER_BOUND('',#1225,.T.);
#853=FACE_OUTER_BOUND('',#1226,.T.);
#854=FACE_OUTER_BOUND('',#1227,.T.);
#855=FACE_OUTER_BOUND('',#1229,.T.);
#1225=EDGE_LOOP('',(#3976,#3977,#3978,#3979));
#1226=EDGE_LOOP('',(#3980,#3981,#3982,#3983));
#1227=EDGE_LOOP('',(#3984));
#1228=EDGE_LOOP('',(#3985));
#1229=EDGE_LOOP('',(#3986));
#1230=EDGE_LOOP('',(#3987));
#1563=LINE('',#7677,#1903);
#1564=LINE('',#7683,#1904);
#1903=VECTOR('',#6426,0.32);
#1904=VECTOR('',#6433,0.6);
#2106=CIRCLE('',#5116,0.32);
#2107=CIRCLE('',#5117,0.32);
#2108=CIRCLE('',#5119,0.6);
#2109=CIRCLE('',#5120,0.6);
#2441=VERTEX_POINT('',#7674);
#2442=VERTEX_POINT('',#7676);
#2443=VERTEX_POINT('',#7680);
#2444=VERTEX_POINT('',#7682);
#2956=EDGE_CURVE('',#2441,#2441,#2106,.T.);
#2957=EDGE_CURVE('',#2441,#2442,#1563,.T.);
#2958=EDGE_CURVE('',#2442,#2442,#2107,.T.);
#2959=EDGE_CURVE('',#2443,#2443,#2108,.T.);
#2960=EDGE_CURVE('',#2443,#2444,#1564,.T.);
#2961=EDGE_CURVE('',#2444,#2444,#2109,.T.);
#3976=ORIENTED_EDGE('',*,*,#2956,.F.);
#3977=ORIENTED_EDGE('',*,*,#2957,.T.);
#3978=ORIENTED_EDGE('',*,*,#2958,.T.);
#3979=ORIENTED_EDGE('',*,*,#2957,.F.);
#3980=ORIENTED_EDGE('',*,*,#2959,.F.);
#3981=ORIENTED_EDGE('',*,*,#2960,.T.);
#3982=ORIENTED_EDGE('',*,*,#2961,.T.);
#3983=ORIENTED_EDGE('',*,*,#2960,.F.);
#3984=ORIENTED_EDGE('',*,*,#2959,.T.);
#3985=ORIENTED_EDGE('',*,*,#2956,.T.);
#3986=ORIENTED_EDGE('',*,*,#2961,.F.);
#3987=ORIENTED_EDGE('',*,*,#2958,.F.);
#4131=CYLINDRICAL_SURFACE('',#5115,0.32);
#4132=CYLINDRICAL_SURFACE('',#5118,0.6);
#4371=ADVANCED_FACE('',(#852),#4131,.F.);
#4372=ADVANCED_FACE('',(#853),#4132,.T.);
#4373=ADVANCED_FACE('',(#854,#456),#603,.T.);
#4374=ADVANCED_FACE('',(#855,#457),#604,.F.);
#4414=CLOSED_SHELL('',(#4371,#4372,#4373,#4374));
#5114=AXIS2_PLACEMENT_3D('',#7672,#6420,#6421);
#5115=AXIS2_PLACEMENT_3D('',#7673,#6422,#6423);
#5116=AXIS2_PLACEMENT_3D('',#7675,#6424,#6425);
#5117=AXIS2_PLACEMENT_3D('',#7678,#6427,#6428);
#5118=AXIS2_PLACEMENT_3D('',#7679,#6429,#6430);
#5119=AXIS2_PLACEMENT_3D('',#7681,#6431,#6432);
#5120=AXIS2_PLACEMENT_3D('',#7684,#6434,#6435);
#5121=AXIS2_PLACEMENT_3D('',#7685,#6436,#6437);
#5122=AXIS2_PLACEMENT_3D('',#7686,#6438,#6439);
#6420=DIRECTION('axis',(0.,0.,1.));
#6421=DIRECTION('refdir',(1.,0.,0.));
#6422=DIRECTION('center_axis',(0.,1.,0.));
#6423=DIRECTION('ref_axis',(1.,0.,0.));
#6424=DIRECTION('center_axis',(0.,-1.,0.));
#6425=DIRECTION('ref_axis',(1.,0.,0.));
#6426=DIRECTION('',(0.,-1.,0.));
#6427=DIRECTION('center_axis',(0.,-1.,0.));
#6428=DIRECTION('ref_axis',(1.,0.,0.));
#6429=DIRECTION('center_axis',(0.,1.,0.));
#6430=DIRECTION('ref_axis',(1.,0.,0.));
#6431=DIRECTION('center_axis',(0.,1.,0.));
#6432=DIRECTION('ref_axis',(1.,0.,0.));
#6433=DIRECTION('',(0.,-1.,0.));
#6434=DIRECTION('center_axis',(0.,1.,0.));
#6435=DIRECTION('ref_axis',(1.,0.,0.));
#6436=DIRECTION('center_axis',(0.,1.,0.));
#6437=DIRECTION('ref_axis',(1.,0.,0.));
#6438=DIRECTION('center_axis',(0.,1.,0.));
#6439=DIRECTION('ref_axis',(1.,0.,0.));
#7672=CARTESIAN_POINT('',(0.,0.,0.));
#7673=CARTESIAN_POINT('Origin',(0.,0.,0.));
#7674=CARTESIAN_POINT('',(-0.32,0.16,3.91886975727153E-17));
#7675=CARTESIAN_POINT('Origin',(0.,0.16,0.));
#7676=CARTESIAN_POINT('',(-0.32,0.,3.91886975727153E-17));
#7677=CARTESIAN_POINT('',(-0.32,0.,3.91886975727153E-17));
#7678=CARTESIAN_POINT('Origin',(0.,0.,0.));
#7679=CARTESIAN_POINT('Origin',(0.,0.,0.));
#7680=CARTESIAN_POINT('',(-0.6,0.16,7.34788079488412E-17));
#7681=CARTESIAN_POINT('Origin',(0.,0.16,0.));
#7682=CARTESIAN_POINT('',(-0.6,0.,7.34788079488412E-17));
#7683=CARTESIAN_POINT('',(-0.6,0.,7.34788079488412E-17));
#7684=CARTESIAN_POINT('Origin',(0.,0.,0.));
#7685=CARTESIAN_POINT('Origin',(0.,0.16,0.));
#7686=CARTESIAN_POINT('Origin',(0.,0.,0.));
#7807=UNCERTAINTY_MEASURE_WITH_UNIT(LENGTH_MEASURE(0.001),#7836,
'DISTANCE_ACCURACY_VALUE',
'Maximum model space distance between geometric entities at asserted c
onnectivities');
#7809=UNCERTAINTY_MEASURE_WITH_UNIT(LENGTH_MEASURE(0.001),#7836,
'DISTANCE_ACCURACY_VALUE',
'Maximum model space distance between geometric entities at asserted c
onnectivities');
#7833=(
GEOMETRIC_REPRESENTATION_CONTEXT(3)
GLOBAL_UNCERTAINTY_ASSIGNED_CONTEXT((#7807))
GLOBAL_UNIT_ASSIGNED_CONTEXT((#7836,#7838,#7839))
REPRESENTATION_CONTEXT('','3D')
);
#7835=(
GEOMETRIC_REPRESENTATION_CONTEXT(3)
GLOBAL_UNCERTAINTY_ASSIGNED_CONTEXT((#7809))
GLOBAL_UNIT_ASSIGNED_CONTEXT((#7836,#7838,#7839))
REPRESENTATION_CONTEXT('','3D')
);
#7836=(
LENGTH_UNIT()
NAMED_UNIT(*)
SI_UNIT(.CENTI.,.METRE.)
);
#7838=(
NAMED_UNIT(*)
PLANE_ANGLE_UNIT()
SI_UNIT($,.RADIAN.)
);
#7839=(
NAMED_UNIT(*)
SI_UNIT($,.STERADIAN.)
SOLID_ANGLE_UNIT()
);
#7863=SHAPE_DEFINITION_REPRESENTATION(#7917,#7969);
#7917=PRODUCT_DEFINITION_SHAPE('',$,#7995);
#7969=SHAPE_REPRESENTATION('',(#5114),#7833);
#7971=PRODUCT_DEFINITION_CONTEXT('part definition',#8048,'design');
#7995=PRODUCT_DEFINITION('Flat Washer - M6','Flat Washer - M6',#8020,#7971);
#8020=PRODUCT_DEFINITION_FORMATION('',$,#8073);
#8048=APPLICATION_CONTEXT(
'Core Data for Automotive Mechanical Design Process');
#8049=PRODUCT_CONTEXT('part definition',#8048,'mechanical');
#8073=PRODUCT('Flat Washer - M6','Flat Washer - M6','Flat Washer - M6',
(#8049));
#8145=COLOUR_RGB('Black',0.12,0.14,0.17);
#8146=FILL_AREA_STYLE_COLOUR('',#8145);
#8147=FILL_AREA_STYLE('',(#8146));
#8148=SURFACE_STYLE_FILL_AREA(#8147);
#8149=SURFACE_SIDE_STYLE('',(#8148));
#8150=SURFACE_STYLE_USAGE(.BOTH.,#8149);
#8151=PRESENTATION_STYLE_ASSIGNMENT((#8150));
ENDSEC;
END-ISO-10303-21;
